ISO-10303-21;
HEADER;
/* Generated by software containing ST-Developer
 * from STEP Tools, Inc. (www.steptools.com) 
 */

FILE_DESCRIPTION(
/* description */ ('PAT-091'),
/* implementation_level */ '2;1');

FILE_NAME(
/* name */ 'Axle end keeper (7).step',
/* time_stamp */ '2026-10-27T15:34:44-07:00',
/* author */ (''),
/* organization */ (''),
/* preprocessor_version */ 'ST-DEVELOPER v20.2',
/* originating_system */ 'Autodesk Translation Framework v15.17.0.0',
/* authorisation */ '');

FILE_SCHEMA (('AUTOMOTIVE_DESIGN { 1 0 10303 214 3 1 1 }'));
ENDSEC;

DATA;
#10=MECHANICAL_DESIGN_GEOMETRIC_PRESENTATION_REPRESENTATION('',(#1019),#25100);
#799=SHAPE_REPRESENTATION_RELATIONSHIP('SRR','None',#25563,#909);
#909=ADVANCED_BREP_SHAPE_REPRESENTATION('',(#1141),#25033);
#1019=STYLED_ITEM('',(#26191),#1141);
#1141=MANIFOLD_SOLID_BREP('Body1',#13298);
#1462=FACE_BOUND('',#3523,.T.);
#1463=FACE_BOUND('',#3525,.T.);
#1859=PLANE('',#15380);
#1860=PLANE('',#15381);
#2455=FACE_OUTER_BOUND('',#3520,.T.);
#2456=FACE_OUTER_BOUND('',#3521,.T.);
#2457=FACE_OUTER_BOUND('',#3522,.T.);
#2458=FACE_OUTER_BOUND('',#3524,.T.);
#3520=EDGE_LOOP('',(#10572,#10573,#10574,#10575));
#3521=EDGE_LOOP('',(#10576,#10577,#10578,#10579));
#3522=EDGE_LOOP('',(#10580));
#3523=EDGE_LOOP('',(#10581));
#3524=EDGE_LOOP('',(#10582));
#3525=EDGE_LOOP('',(#10583));
#4577=LINE('',#22807,#5317);
#4578=LINE('',#22813,#5318);
#5317=VECTOR('',#18503,0.225000000000001);
#5318=VECTOR('',#18510,1.);
#5947=CIRCLE('',#15375,0.225000000000001);
#5948=CIRCLE('',#15376,0.225000000000001);
#5949=CIRCLE('',#15378,1.);
#5950=CIRCLE('',#15379,1.);
#6914=VERTEX_POINT('',#22804);
#6915=VERTEX_POINT('',#22806);
#6916=VERTEX_POINT('',#22810);
#6917=VERTEX_POINT('',#22812);
#8221=EDGE_CURVE('',#6914,#6914,#5947,.T.);
#8222=EDGE_CURVE('',#6914,#6915,#4577,.T.);
#8223=EDGE_CURVE('',#6915,#6915,#5948,.T.);
#8224=EDGE_CURVE('',#6916,#6916,#5949,.T.);
#8225=EDGE_CURVE('',#6916,#6917,#4578,.T.);
#8226=EDGE_CURVE('',#6917,#6917,#5950,.T.);
#10572=ORIENTED_EDGE('',*,*,#8221,.F.);
#10573=ORIENTED_EDGE('',*,*,#8222,.T.);
#10574=ORIENTED_EDGE('',*,*,#8223,.T.);
#10575=ORIENTED_EDGE('',*,*,#8222,.F.);
#10576=ORIENTED_EDGE('',*,*,#8224,.F.);
#10577=ORIENTED_EDGE('',*,*,#8225,.T.);
#10578=ORIENTED_EDGE('',*,*,#8226,.T.);
#10579=ORIENTED_EDGE('',*,*,#8225,.F.);
#10580=ORIENTED_EDGE('',*,*,#8224,.T.);
#10581=ORIENTED_EDGE('',*,*,#8221,.T.);
#10582=ORIENTED_EDGE('',*,*,#8226,.F.);
#10583=ORIENTED_EDGE('',*,*,#8223,.F.);
#12240=CYLINDRICAL_SURFACE('',#15374,0.225000000000001);
#12241=CYLINDRICAL_SURFACE('',#15377,1.);
#12822=ADVANCED_FACE('',(#2455),#12240,.F.);
#12823=ADVANCED_FACE('',(#2456),#12241,.T.);
#12824=ADVANCED_FACE('',(#2457,#1462),#1859,.T.);
#12825=ADVANCED_FACE('',(#2458,#1463),#1860,.F.);
#13298=CLOSED_SHELL('',(#12822,#12823,#12824,#12825));
#15373=AXIS2_PLACEMENT_3D('',#22802,#18497,#18498);
#15374=AXIS2_PLACEMENT_3D('',#22803,#18499,#18500);
#15375=AXIS2_PLACEMENT_3D('',#22805,#18501,#18502);
#15376=AXIS2_PLACEMENT_3D('',#22808,#18504,#18505);
#15377=AXIS2_PLACEMENT_3D('',#22809,#18506,#18507);
#15378=AXIS2_PLACEMENT_3D('',#22811,#18508,#18509);
#15379=AXIS2_PLACEMENT_3D('',#22814,#18511,#18512);
#15380=AXIS2_PLACEMENT_3D('',#22815,#18513,#18514);
#15381=AXIS2_PLACEMENT_3D('',#22816,#18515,#18516);
#18497=DIRECTION('axis',(0.,0.,1.));
#18498=DIRECTION('refdir',(1.,0.,0.));
#18499=DIRECTION('center_axis',(0.,1.,0.));
#18500=DIRECTION('ref_axis',(1.,0.,0.));
#18501=DIRECTION('center_axis',(0.,-1.,0.));
#18502=DIRECTION('ref_axis',(1.,0.,0.));
#18503=DIRECTION('',(0.,-1.,0.));
#18504=DIRECTION('center_axis',(0.,-1.,0.));
#18505=DIRECTION('ref_axis',(1.,0.,0.));
#18506=DIRECTION('center_axis',(0.,1.,0.));
#18507=DIRECTION('ref_axis',(1.,0.,0.));
#18508=DIRECTION('center_axis',(0.,1.,0.));
#18509=DIRECTION('ref_axis',(1.,0.,0.));
#18510=DIRECTION('',(0.,-1.,0.));
#18511=DIRECTION('center_axis',(0.,1.,0.));
#18512=DIRECTION('ref_axis',(1.,0.,0.));
#18513=DIRECTION('center_axis',(0.,1.,0.));
#18514=DIRECTION('ref_axis',(1.,0.,0.));
#18515=DIRECTION('center_axis',(0.,1.,0.));
#18516=DIRECTION('ref_axis',(1.,0.,0.));
#22802=CARTESIAN_POINT('',(0.,0.,0.));
#22803=CARTESIAN_POINT('Origin',(38.7298334620742,6.5,13.));
#22804=CARTESIAN_POINT('',(38.5048334620742,6.7,13.));
#22805=CARTESIAN_POINT('Origin',(38.7298334620742,6.7,13.));
#22806=CARTESIAN_POINT('',(38.5048334620742,6.5,13.));
#22807=CARTESIAN_POINT('',(38.5048334620742,6.5,13.));
#22808=CARTESIAN_POINT('Origin',(38.7298334620742,6.5,13.));
#22809=CARTESIAN_POINT('Origin',(38.7298334620742,6.5,13.));
#22810=CARTESIAN_POINT('',(37.7298334620742,6.7,13.));
#22811=CARTESIAN_POINT('Origin',(38.7298334620742,6.7,13.));
#22812=CARTESIAN_POINT('',(37.7298334620742,6.5,13.));
#22813=CARTESIAN_POINT('',(37.7298334620742,6.5,13.));
#22814=CARTESIAN_POINT('Origin',(38.7298334620742,6.5,13.));
#22815=CARTESIAN_POINT('Origin',(38.7298334620742,6.7,13.));
#22816=CARTESIAN_POINT('Origin',(38.7298334620742,6.5,13.));
#24912=UNCERTAINTY_MEASURE_WITH_UNIT(LENGTH_MEASURE(0.001),#25101,
'DISTANCE_ACCURACY_VALUE',
'Maximum model space distance between geometric entities at asserted c
onnectivities');
#24979=UNCERTAINTY_MEASURE_WITH_UNIT(LENGTH_MEASURE(0.001),#25101,
'DISTANCE_ACCURACY_VALUE',
'Maximum model space distance between geometric entities at asserted c
onnectivities');
#25033=(
GEOMETRIC_REPRESENTATION_CONTEXT(3)
GLOBAL_UNCERTAINTY_ASSIGNED_CONTEXT((#24912))
GLOBAL_UNIT_ASSIGNED_CONTEXT((#25101,#25103,#25104))
REPRESENTATION_CONTEXT('','3D')
);
#25100=(
GEOMETRIC_REPRESENTATION_CONTEXT(3)
GLOBAL_UNCERTAINTY_ASSIGNED_CONTEXT((#24979))
GLOBAL_UNIT_ASSIGNED_CONTEXT((#25101,#25103,#25104))
REPRESENTATION_CONTEXT('','3D')
);
#25101=(
LENGTH_UNIT()
NAMED_UNIT(*)
SI_UNIT(.CENTI.,.METRE.)
);
#25103=(
NAMED_UNIT(*)
PLANE_ANGLE_UNIT()
SI_UNIT($,.RADIAN.)
);
#25104=(
NAMED_UNIT(*)
SI_UNIT($,.STERADIAN.)
SOLID_ANGLE_UNIT()
);
#25158=SHAPE_DEFINITION_REPRESENTATION(#25278,#25563);
#25278=PRODUCT_DEFINITION_SHAPE('',$,#25684);
#25563=SHAPE_REPRESENTATION('',(#15373),#25033);
#25630=PRODUCT_DEFINITION_CONTEXT('part definition',#25992,'design');
#25684=PRODUCT_DEFINITION('Axle end keeper (7)','Axle end keeper (7)',#25804,
#25630);
#25804=PRODUCT_DEFINITION_FORMATION('',$,#26047);
#25992=APPLICATION_CONTEXT(
'Core Data for Automotive Mechanical Design Process');
#25993=PRODUCT_CONTEXT('part definition',#25992,'mechanical');
#26047=PRODUCT('Axle end keeper (7)','Axle end keeper (7)',
'Axle end keeper (7)',(#25993));
#26185=COLOUR_RGB('Grey',0.48,0.52,0.57);
#26186=FILL_AREA_STYLE_COLOUR('',#26185);
#26187=FILL_AREA_STYLE('',(#26186));
#26188=SURFACE_STYLE_FILL_AREA(#26187);
#26189=SURFACE_SIDE_STYLE('',(#26188));
#26190=SURFACE_STYLE_USAGE(.BOTH.,#26189);
#26191=PRESENTATION_STYLE_ASSIGNMENT((#26190));
ENDSEC;
END-ISO-10303-21;
